ISO-10303-21;
HEADER;
/* Generated by software containing ST-Developer
 * from STEP Tools, Inc. (www.steptools.com) 
 */

FILE_DESCRIPTION(
/* description */ ('Gravity roller conveyor section'),
/* implementation_level */ '2;1');

FILE_NAME(
/* name */ 'M4x10 Cap Screw.step',
/* time_stamp */ '2026-11-02T07:43:02-08:00',
/* author */ (''),
/* organization */ (''),
/* preprocessor_version */ 'ST-DEVELOPER v20.2',
/* originating_system */ 'Autodesk Translation Framework v15.17.0.0',
/* authorisation */ '');

FILE_SCHEMA (('AUTOMOTIVE_DESIGN { 1 0 10303 214 3 1 1 }'));
ENDSEC;

DATA;
#10=MECHANICAL_DESIGN_GEOMETRIC_PRESENTATION_REPRESENTATION('',(#566),#13821);
#419=CONICAL_SURFACE('',#8639,0.325,0.785398163397448);
#420=CONICAL_SURFACE('',#8643,0.335,0.785398163397448);
#421=CONICAL_SURFACE('',#8647,0.21,0.463647609000806);
#427=ORIENTED_CLOSED_SHELL('',*,#7666,.F.);
#431=BREP_WITH_VOIDS('Body1',#7667,(#427));
#490=SHAPE_REPRESENTATION_RELATIONSHIP('SRR','None',#14029,#524);
#524=ADVANCED_BREP_SHAPE_REPRESENTATION('',(#431),#13816);
#566=STYLED_ITEM('',(#14193),#431);
#689=FACE_BOUND('',#1876,.T.);
#962=PLANE('',#8627);
#963=PLANE('',#8628);
#964=PLANE('',#8629);
#965=PLANE('',#8630);
#966=PLANE('',#8631);
#967=PLANE('',#8632);
#968=PLANE('',#8633);
#969=PLANE('',#8634);
#970=PLANE('',#8635);
#971=PLANE('',#8637);
#972=PLANE('',#8645);
#1363=FACE_OUTER_BOUND('',#1862,.T.);
#1364=FACE_OUTER_BOUND('',#1863,.T.);
#1365=FACE_OUTER_BOUND('',#1864,.T.);
#1366=FACE_OUTER_BOUND('',#1865,.T.);
#1367=FACE_OUTER_BOUND('',#1866,.T.);
#1368=FACE_OUTER_BOUND('',#1867,.T.);
#1369=FACE_OUTER_BOUND('',#1868,.T.);
#1370=FACE_OUTER_BOUND('',#1869,.T.);
#1371=FACE_OUTER_BOUND('',#1870,.T.);
#1372=FACE_OUTER_BOUND('',#1871,.T.);
#1373=FACE_OUTER_BOUND('',#1872,.T.);
#1374=FACE_OUTER_BOUND('',#1873,.T.);
#1375=FACE_OUTER_BOUND('',#1874,.T.);
#1376=FACE_OUTER_BOUND('',#1875,.T.);
#1377=FACE_OUTER_BOUND('',#1877,.T.);
#1378=FACE_OUTER_BOUND('',#1878,.T.);
#1862=EDGE_LOOP('',(#6866,#6867,#6868,#6869));
#1863=EDGE_LOOP('',(#6870,#6871,#6872,#6873));
#1864=EDGE_LOOP('',(#6874,#6875,#6876,#6877));
#1865=EDGE_LOOP('',(#6878,#6879,#6880,#6881));
#1866=EDGE_LOOP('',(#6882,#6883,#6884,#6885));
#1867=EDGE_LOOP('',(#6886,#6887,#6888,#6889));
#1868=EDGE_LOOP('',(#6890,#6891,#6892,#6893,#6894,#6895));
#1869=EDGE_LOOP('',(#6896,#6897,#6898,#6899,#6900,#6901));
#1870=EDGE_LOOP('',(#6902));
#1871=EDGE_LOOP('',(#6903));
#1872=EDGE_LOOP('',(#6904,#6905,#6906,#6907));
#1873=EDGE_LOOP('',(#6908,#6909,#6910,#6911));
#1874=EDGE_LOOP('',(#6912,#6913,#6914,#6915));
#1875=EDGE_LOOP('',(#6916));
#1876=EDGE_LOOP('',(#6917));
#1877=EDGE_LOOP('',(#6918,#6919,#6920,#6921));
#1878=EDGE_LOOP('',(#6922,#6923,#6924,#6925));
#2558=LINE('',#13373,#3276);
#2559=LINE('',#13375,#3277);
#2560=LINE('',#13377,#3278);
#2561=LINE('',#13378,#3279);
#2562=LINE('',#13381,#3280);
#2563=LINE('',#13383,#3281);
#2564=LINE('',#13384,#3282);
#2565=LINE('',#13387,#3283);
#2566=LINE('',#13389,#3284);
#2567=LINE('',#13390,#3285);
#2568=LINE('',#13393,#3286);
#2569=LINE('',#13395,#3287);
#2570=LINE('',#13396,#3288);
#2571=LINE('',#13399,#3289);
#2572=LINE('',#13401,#3290);
#2573=LINE('',#13402,#3291);
#2574=LINE('',#13404,#3292);
#2575=LINE('',#13405,#3293);
#2576=LINE('',#13417,#3294);
#2577=LINE('',#13421,#3295);
#2578=LINE('',#13425,#3296);
#2579=LINE('',#13432,#3297);
#2580=LINE('',#13434,#3298);
#3276=VECTOR('',#10597,1.);
#3277=VECTOR('',#10598,1.);
#3278=VECTOR('',#10599,1.);
#3279=VECTOR('',#10600,1.);
#3280=VECTOR('',#10603,1.);
#3281=VECTOR('',#10604,1.);
#3282=VECTOR('',#10605,1.);
#3283=VECTOR('',#10608,1.);
#3284=VECTOR('',#10609,1.);
#3285=VECTOR('',#10610,1.);
#3286=VECTOR('',#10613,1.);
#3287=VECTOR('',#10614,1.);
#3288=VECTOR('',#10615,1.);
#3289=VECTOR('',#10618,1.);
#3290=VECTOR('',#10619,1.);
#3291=VECTOR('',#10620,1.);
#3292=VECTOR('',#10623,1.);
#3293=VECTOR('',#10624,1.);
#3294=VECTOR('',#10641,0.325);
#3295=VECTOR('',#10646,0.35);
#3296=VECTOR('',#10651,0.335);
#3297=VECTOR('',#10660,0.21);
#3298=VECTOR('',#10663,0.2);
#3558=CIRCLE('',#8636,0.1954);
#3559=CIRCLE('',#8638,0.3);
#3560=CIRCLE('',#8640,0.35);
#3561=CIRCLE('',#8642,0.35);
#3562=CIRCLE('',#8644,0.32);
#3563=CIRCLE('',#8646,0.22);
#3564=CIRCLE('',#8648,0.1954);
#4152=VERTEX_POINT('',#13371);
#4153=VERTEX_POINT('',#13372);
#4154=VERTEX_POINT('',#13374);
#4155=VERTEX_POINT('',#13376);
#4156=VERTEX_POINT('',#13380);
#4157=VERTEX_POINT('',#13382);
#4158=VERTEX_POINT('',#13386);
#4159=VERTEX_POINT('',#13388);
#4160=VERTEX_POINT('',#13392);
#4161=VERTEX_POINT('',#13394);
#4162=VERTEX_POINT('',#13398);
#4163=VERTEX_POINT('',#13400);
#4164=VERTEX_POINT('',#13409);
#4165=VERTEX_POINT('',#13412);
#4166=VERTEX_POINT('',#13415);
#4167=VERTEX_POINT('',#13419);
#4168=VERTEX_POINT('',#13423);
#4169=VERTEX_POINT('',#13427);
#4170=VERTEX_POINT('',#13430);
#5070=EDGE_CURVE('',#4152,#4153,#2558,.T.);
#5071=EDGE_CURVE('',#4153,#4154,#2559,.T.);
#5072=EDGE_CURVE('',#4154,#4155,#2560,.T.);
#5073=EDGE_CURVE('',#4152,#4155,#2561,.T.);
#5074=EDGE_CURVE('',#4153,#4156,#2562,.T.);
#5075=EDGE_CURVE('',#4156,#4157,#2563,.T.);
#5076=EDGE_CURVE('',#4157,#4154,#2564,.T.);
#5077=EDGE_CURVE('',#4156,#4158,#2565,.T.);
#5078=EDGE_CURVE('',#4158,#4159,#2566,.T.);
#5079=EDGE_CURVE('',#4159,#4157,#2567,.T.);
#5080=EDGE_CURVE('',#4158,#4160,#2568,.T.);
#5081=EDGE_CURVE('',#4160,#4161,#2569,.T.);
#5082=EDGE_CURVE('',#4161,#4159,#2570,.T.);
#5083=EDGE_CURVE('',#4160,#4162,#2571,.T.);
#5084=EDGE_CURVE('',#4162,#4163,#2572,.T.);
#5085=EDGE_CURVE('',#4163,#4161,#2573,.T.);
#5086=EDGE_CURVE('',#4162,#4152,#2574,.T.);
#5087=EDGE_CURVE('',#4155,#4163,#2575,.T.);
#5088=EDGE_CURVE('',#4164,#4164,#3558,.T.);
#5089=EDGE_CURVE('',#4165,#4165,#3559,.T.);
#5090=EDGE_CURVE('',#4166,#4166,#3560,.T.);
#5091=EDGE_CURVE('',#4166,#4165,#2576,.T.);
#5092=EDGE_CURVE('',#4167,#4167,#3561,.T.);
#5093=EDGE_CURVE('',#4167,#4166,#2577,.T.);
#5094=EDGE_CURVE('',#4168,#4168,#3562,.T.);
#5095=EDGE_CURVE('',#4168,#4167,#2578,.T.);
#5096=EDGE_CURVE('',#4169,#4169,#3563,.T.);
#5097=EDGE_CURVE('',#4170,#4170,#3564,.F.);
#5098=EDGE_CURVE('',#4170,#4169,#2579,.T.);
#5099=EDGE_CURVE('',#4164,#4170,#2580,.T.);
#6866=ORIENTED_EDGE('',*,*,#5070,.T.);
#6867=ORIENTED_EDGE('',*,*,#5071,.T.);
#6868=ORIENTED_EDGE('',*,*,#5072,.T.);
#6869=ORIENTED_EDGE('',*,*,#5073,.F.);
#6870=ORIENTED_EDGE('',*,*,#5074,.T.);
#6871=ORIENTED_EDGE('',*,*,#5075,.T.);
#6872=ORIENTED_EDGE('',*,*,#5076,.T.);
#6873=ORIENTED_EDGE('',*,*,#5071,.F.);
#6874=ORIENTED_EDGE('',*,*,#5077,.T.);
#6875=ORIENTED_EDGE('',*,*,#5078,.T.);
#6876=ORIENTED_EDGE('',*,*,#5079,.T.);
#6877=ORIENTED_EDGE('',*,*,#5075,.F.);
#6878=ORIENTED_EDGE('',*,*,#5080,.T.);
#6879=ORIENTED_EDGE('',*,*,#5081,.T.);
#6880=ORIENTED_EDGE('',*,*,#5082,.T.);
#6881=ORIENTED_EDGE('',*,*,#5078,.F.);
#6882=ORIENTED_EDGE('',*,*,#5083,.T.);
#6883=ORIENTED_EDGE('',*,*,#5084,.T.);
#6884=ORIENTED_EDGE('',*,*,#5085,.T.);
#6885=ORIENTED_EDGE('',*,*,#5081,.F.);
#6886=ORIENTED_EDGE('',*,*,#5086,.T.);
#6887=ORIENTED_EDGE('',*,*,#5073,.T.);
#6888=ORIENTED_EDGE('',*,*,#5087,.T.);
#6889=ORIENTED_EDGE('',*,*,#5084,.F.);
#6890=ORIENTED_EDGE('',*,*,#5086,.F.);
#6891=ORIENTED_EDGE('',*,*,#5083,.F.);
#6892=ORIENTED_EDGE('',*,*,#5080,.F.);
#6893=ORIENTED_EDGE('',*,*,#5077,.F.);
#6894=ORIENTED_EDGE('',*,*,#5074,.F.);
#6895=ORIENTED_EDGE('',*,*,#5070,.F.);
#6896=ORIENTED_EDGE('',*,*,#5087,.F.);
#6897=ORIENTED_EDGE('',*,*,#5072,.F.);
#6898=ORIENTED_EDGE('',*,*,#5076,.F.);
#6899=ORIENTED_EDGE('',*,*,#5079,.F.);
#6900=ORIENTED_EDGE('',*,*,#5082,.F.);
#6901=ORIENTED_EDGE('',*,*,#5085,.F.);
#6902=ORIENTED_EDGE('',*,*,#5088,.F.);
#6903=ORIENTED_EDGE('',*,*,#5089,.F.);
#6904=ORIENTED_EDGE('',*,*,#5090,.F.);
#6905=ORIENTED_EDGE('',*,*,#5091,.T.);
#6906=ORIENTED_EDGE('',*,*,#5089,.T.);
#6907=ORIENTED_EDGE('',*,*,#5091,.F.);
#6908=ORIENTED_EDGE('',*,*,#5092,.F.);
#6909=ORIENTED_EDGE('',*,*,#5093,.T.);
#6910=ORIENTED_EDGE('',*,*,#5090,.T.);
#6911=ORIENTED_EDGE('',*,*,#5093,.F.);
#6912=ORIENTED_EDGE('',*,*,#5094,.F.);
#6913=ORIENTED_EDGE('',*,*,#5095,.T.);
#6914=ORIENTED_EDGE('',*,*,#5092,.T.);
#6915=ORIENTED_EDGE('',*,*,#5095,.F.);
#6916=ORIENTED_EDGE('',*,*,#5094,.T.);
#6917=ORIENTED_EDGE('',*,*,#5096,.F.);
#6918=ORIENTED_EDGE('',*,*,#5097,.F.);
#6919=ORIENTED_EDGE('',*,*,#5098,.T.);
#6920=ORIENTED_EDGE('',*,*,#5096,.T.);
#6921=ORIENTED_EDGE('',*,*,#5098,.F.);
#6922=ORIENTED_EDGE('',*,*,#5088,.T.);
#6923=ORIENTED_EDGE('',*,*,#5099,.T.);
#6924=ORIENTED_EDGE('',*,*,#5097,.T.);
#6925=ORIENTED_EDGE('',*,*,#5099,.F.);
#7196=CYLINDRICAL_SURFACE('',#8641,0.35);
#7197=CYLINDRICAL_SURFACE('',#8649,0.1954);
#7564=ADVANCED_FACE('',(#1363),#962,.F.);
#7565=ADVANCED_FACE('',(#1364),#963,.F.);
#7566=ADVANCED_FACE('',(#1365),#964,.F.);
#7567=ADVANCED_FACE('',(#1366),#965,.F.);
#7568=ADVANCED_FACE('',(#1367),#966,.F.);
#7569=ADVANCED_FACE('',(#1368),#967,.F.);
#7570=ADVANCED_FACE('',(#1369),#968,.F.);
#7571=ADVANCED_FACE('',(#1370),#969,.F.);
#7572=ADVANCED_FACE('',(#1371),#970,.F.);
#7573=ADVANCED_FACE('',(#1372),#971,.T.);
#7574=ADVANCED_FACE('',(#1373),#419,.T.);
#7575=ADVANCED_FACE('',(#1374),#7196,.T.);
#7576=ADVANCED_FACE('',(#1375),#420,.T.);
#7577=ADVANCED_FACE('',(#1376,#689),#972,.T.);
#7578=ADVANCED_FACE('',(#1377),#421,.T.);
#7579=ADVANCED_FACE('',(#1378),#7197,.T.);
#7666=CLOSED_SHELL('',(#7564,#7565,#7566,#7567,#7568,#7569,#7570,#7571));
#7667=CLOSED_SHELL('',(#7572,#7573,#7574,#7575,#7576,#7577,#7578,#7579));
#8626=AXIS2_PLACEMENT_3D('',#13369,#10593,#10594);
#8627=AXIS2_PLACEMENT_3D('',#13370,#10595,#10596);
#8628=AXIS2_PLACEMENT_3D('',#13379,#10601,#10602);
#8629=AXIS2_PLACEMENT_3D('',#13385,#10606,#10607);
#8630=AXIS2_PLACEMENT_3D('',#13391,#10611,#10612);
#8631=AXIS2_PLACEMENT_3D('',#13397,#10616,#10617);
#8632=AXIS2_PLACEMENT_3D('',#13403,#10621,#10622);
#8633=AXIS2_PLACEMENT_3D('',#13406,#10625,#10626);
#8634=AXIS2_PLACEMENT_3D('',#13407,#10627,#10628);
#8635=AXIS2_PLACEMENT_3D('',#13408,#10629,#10630);
#8636=AXIS2_PLACEMENT_3D('',#13410,#10631,#10632);
#8637=AXIS2_PLACEMENT_3D('',#13411,#10633,#10634);
#8638=AXIS2_PLACEMENT_3D('',#13413,#10635,#10636);
#8639=AXIS2_PLACEMENT_3D('',#13414,#10637,#10638);
#8640=AXIS2_PLACEMENT_3D('',#13416,#10639,#10640);
#8641=AXIS2_PLACEMENT_3D('',#13418,#10642,#10643);
#8642=AXIS2_PLACEMENT_3D('',#13420,#10644,#10645);
#8643=AXIS2_PLACEMENT_3D('',#13422,#10647,#10648);
#8644=AXIS2_PLACEMENT_3D('',#13424,#10649,#10650);
#8645=AXIS2_PLACEMENT_3D('',#13426,#10652,#10653);
#8646=AXIS2_PLACEMENT_3D('',#13428,#10654,#10655);
#8647=AXIS2_PLACEMENT_3D('',#13429,#10656,#10657);
#8648=AXIS2_PLACEMENT_3D('',#13431,#10658,#10659);
#8649=AXIS2_PLACEMENT_3D('',#13433,#10661,#10662);
#10593=DIRECTION('axis',(0.,0.,1.));
#10594=DIRECTION('refdir',(1.,0.,0.));
#10595=DIRECTION('center_axis',(0.866025403784439,0.,-0.5));
#10596=DIRECTION('ref_axis',(0.5,0.,0.866025403784439));
#10597=DIRECTION('',(-0.5,0.,-0.866025403784439));
#10598=DIRECTION('',(0.,-1.,0.));
#10599=DIRECTION('',(0.5,0.,0.866025403784439));
#10600=DIRECTION('',(0.,-1.,0.));
#10601=DIRECTION('center_axis',(1.60246890531964E-16,0.,-1.));
#10602=DIRECTION('ref_axis',(1.,0.,1.60246890531964E-16));
#10603=DIRECTION('',(-1.,0.,-1.60246890531964E-16));
#10604=DIRECTION('',(0.,-1.,0.));
#10605=DIRECTION('',(1.,0.,1.60246890531964E-16));
#10606=DIRECTION('center_axis',(-0.866025403784439,0.,-0.5));
#10607=DIRECTION('ref_axis',(0.5,0.,-0.866025403784439));
#10608=DIRECTION('',(-0.5,0.,0.866025403784439));
#10609=DIRECTION('',(0.,-1.,0.));
#10610=DIRECTION('',(0.5,0.,-0.866025403784439));
#10611=DIRECTION('center_axis',(-0.866025403784439,0.,0.5));
#10612=DIRECTION('ref_axis',(-0.5,0.,-0.866025403784439));
#10613=DIRECTION('',(0.5,0.,0.866025403784439));
#10614=DIRECTION('',(0.,-1.,0.));
#10615=DIRECTION('',(-0.5,0.,-0.866025403784439));
#10616=DIRECTION('center_axis',(-1.60246890531964E-16,0.,1.));
#10617=DIRECTION('ref_axis',(-1.,0.,-1.60246890531964E-16));
#10618=DIRECTION('',(1.,0.,1.60246890531964E-16));
#10619=DIRECTION('',(0.,-1.,0.));
#10620=DIRECTION('',(-1.,0.,-1.60246890531964E-16));
#10621=DIRECTION('center_axis',(0.866025403784439,0.,0.5));
#10622=DIRECTION('ref_axis',(-0.5,0.,0.866025403784439));
#10623=DIRECTION('',(0.5,0.,-0.866025403784439));
#10624=DIRECTION('',(-0.5,0.,0.866025403784439));
#10625=DIRECTION('center_axis',(0.,1.,0.));
#10626=DIRECTION('ref_axis',(1.,0.,0.));
#10627=DIRECTION('center_axis',(0.,-1.,0.));
#10628=DIRECTION('ref_axis',(0.,0.,-1.));
#10629=DIRECTION('center_axis',(0.,1.,0.));
#10630=DIRECTION('ref_axis',(1.,0.,0.));
#10631=DIRECTION('center_axis',(0.,1.,0.));
#10632=DIRECTION('ref_axis',(1.,0.,0.));
#10633=DIRECTION('center_axis',(0.,1.,0.));
#10634=DIRECTION('ref_axis',(0.,0.,1.));
#10635=DIRECTION('center_axis',(0.,-1.,0.));
#10636=DIRECTION('ref_axis',(1.,0.,0.));
#10637=DIRECTION('center_axis',(0.,-1.,0.));
#10638=DIRECTION('ref_axis',(1.,0.,0.));
#10639=DIRECTION('center_axis',(0.,-1.,0.));
#10640=DIRECTION('ref_axis',(1.,0.,0.));
#10641=DIRECTION('',(0.707106781186547,0.707106781186548,8.65956056235493E-17));
#10642=DIRECTION('center_axis',(0.,-1.,0.));
#10643=DIRECTION('ref_axis',(1.,0.,0.));
#10644=DIRECTION('center_axis',(0.,-1.,0.));
#10645=DIRECTION('ref_axis',(1.,0.,0.));
#10646=DIRECTION('',(0.,1.,0.));
#10647=DIRECTION('center_axis',(0.,1.,0.));
#10648=DIRECTION('ref_axis',(1.,0.,0.));
#10649=DIRECTION('center_axis',(0.,-1.,0.));
#10650=DIRECTION('ref_axis',(1.,0.,0.));
#10651=DIRECTION('',(-0.707106781186547,0.707106781186548,-8.65956056235493E-17));
#10652=DIRECTION('center_axis',(0.,-1.,0.));
#10653=DIRECTION('ref_axis',(0.,0.,-1.));
#10654=DIRECTION('center_axis',(0.,-1.,0.));
#10655=DIRECTION('ref_axis',(1.,0.,0.));
#10656=DIRECTION('center_axis',(0.,1.,0.));
#10657=DIRECTION('ref_axis',(1.,0.,0.));
#10658=DIRECTION('center_axis',(0.,1.,0.));
#10659=DIRECTION('ref_axis',(1.,0.,0.));
#10660=DIRECTION('',(-0.447213595499958,0.894427190999916,-5.47678698264203E-17));
#10661=DIRECTION('center_axis',(0.,-1.,0.));
#10662=DIRECTION('ref_axis',(1.,0.,0.));
#10663=DIRECTION('',(0.,1.,0.));
#13369=CARTESIAN_POINT('',(0.,0.,0.));
#13370=CARTESIAN_POINT('Origin',(0.0866025403784439,-0.4,-0.15));
#13371=CARTESIAN_POINT('',(0.173205080756888,-0.4,0.));
#13372=CARTESIAN_POINT('',(0.0866025403784439,-0.4,-0.15));
#13373=CARTESIAN_POINT('',(0.173205080756888,-0.4,0.));
#13374=CARTESIAN_POINT('',(0.0866025403784439,-0.64,-0.15));
#13375=CARTESIAN_POINT('',(0.0866025403784439,-0.4,-0.15));
#13376=CARTESIAN_POINT('',(0.173205080756888,-0.64,0.));
#13377=CARTESIAN_POINT('',(0.173205080756888,-0.64,0.));
#13378=CARTESIAN_POINT('',(0.173205080756888,-0.4,0.));
#13379=CARTESIAN_POINT('Origin',(-0.0866025403784438,-0.4,-0.15));
#13380=CARTESIAN_POINT('',(-0.0866025403784438,-0.4,-0.15));
#13381=CARTESIAN_POINT('',(0.0866025403784439,-0.4,-0.15));
#13382=CARTESIAN_POINT('',(-0.0866025403784438,-0.64,-0.15));
#13383=CARTESIAN_POINT('',(-0.0866025403784438,-0.4,-0.15));
#13384=CARTESIAN_POINT('',(0.0866025403784439,-0.64,-0.15));
#13385=CARTESIAN_POINT('Origin',(-0.173205080756888,-0.4,-2.77555756156289E-17));
#13386=CARTESIAN_POINT('',(-0.173205080756888,-0.4,-2.12115047744981E-17));
#13387=CARTESIAN_POINT('',(-0.0866025403784438,-0.4,-0.15));
#13388=CARTESIAN_POINT('',(-0.173205080756888,-0.64,-2.77555756156289E-17));
#13389=CARTESIAN_POINT('',(-0.173205080756888,-0.4,-2.12115047744981E-17));
#13390=CARTESIAN_POINT('',(-0.0866025403784438,-0.64,-0.15));
#13391=CARTESIAN_POINT('Origin',(-0.0866025403784439,-0.4,0.15));
#13392=CARTESIAN_POINT('',(-0.0866025403784439,-0.4,0.15));
#13393=CARTESIAN_POINT('',(-0.173205080756888,-0.4,-2.12115047744981E-17));
#13394=CARTESIAN_POINT('',(-0.0866025403784439,-0.64,0.15));
#13395=CARTESIAN_POINT('',(-0.0866025403784439,-0.4,0.15));
#13396=CARTESIAN_POINT('',(-0.173205080756888,-0.64,-2.12115047744981E-17));
#13397=CARTESIAN_POINT('Origin',(0.0866025403784439,-0.4,0.15));
#13398=CARTESIAN_POINT('',(0.0866025403784439,-0.4,0.15));
#13399=CARTESIAN_POINT('',(-0.0866025403784439,-0.4,0.15));
#13400=CARTESIAN_POINT('',(0.0866025403784439,-0.64,0.15));
#13401=CARTESIAN_POINT('',(0.0866025403784439,-0.4,0.15));
#13402=CARTESIAN_POINT('',(-0.0866025403784439,-0.64,0.15));
#13403=CARTESIAN_POINT('Origin',(0.173205080756888,-0.4,0.));
#13404=CARTESIAN_POINT('',(0.0866025403784439,-0.4,0.15));
#13405=CARTESIAN_POINT('',(0.0866025403784439,-0.64,0.15));
#13406=CARTESIAN_POINT('Origin',(0.,-0.4,-2.77555756156289E-17));
#13407=CARTESIAN_POINT('Origin',(0.,-0.64,-2.77555756156289E-17));
#13408=CARTESIAN_POINT('Origin',(0.,-1.,0.));
#13409=CARTESIAN_POINT('',(-0.1954,-1.,2.39295984553393E-17));
#13410=CARTESIAN_POINT('Origin',(0.,-1.,0.));
#13411=CARTESIAN_POINT('Origin',(0.3,0.4,0.));
#13412=CARTESIAN_POINT('',(-0.3,0.4,-3.67394039744206E-17));
#13413=CARTESIAN_POINT('Origin',(0.,0.4,0.));
#13414=CARTESIAN_POINT('Origin',(0.,0.375,0.));
#13415=CARTESIAN_POINT('',(-0.35,0.35,-4.28626379701573E-17));
#13416=CARTESIAN_POINT('Origin',(0.,0.35,0.));
#13417=CARTESIAN_POINT('',(-0.325,0.375,-3.9801020972289E-17));
#13418=CARTESIAN_POINT('Origin',(0.,0.19,0.));
#13419=CARTESIAN_POINT('',(-0.35,0.03,-4.28626379701574E-17));
#13420=CARTESIAN_POINT('Origin',(0.,0.03,0.));
#13421=CARTESIAN_POINT('',(-0.35,0.19,-4.28626379701574E-17));
#13422=CARTESIAN_POINT('Origin',(0.,0.0149999999999999,0.));
#13423=CARTESIAN_POINT('',(-0.32,-3.29597460435593E-17,-3.91886975727153E-17));
#13424=CARTESIAN_POINT('Origin',(0.,0.,0.));
#13425=CARTESIAN_POINT('',(-0.335,0.0149999999999999,-4.10256677714363E-17));
#13426=CARTESIAN_POINT('Origin',(0.22,0.,0.));
#13427=CARTESIAN_POINT('',(-0.22,-6.93889390390723E-18,-2.69422295812418E-17));
#13428=CARTESIAN_POINT('Origin',(0.,0.,0.));
#13429=CARTESIAN_POINT('Origin',(0.,-0.02,0.));
#13430=CARTESIAN_POINT('',(-0.1954,-0.0492,2.39295984553393E-17));
#13431=CARTESIAN_POINT('Origin',(0.,-0.0492,0.));
#13432=CARTESIAN_POINT('',(-0.21,-0.02,-2.57175827820944E-17));
#13433=CARTESIAN_POINT('Origin',(0.,-0.8,0.));
#13434=CARTESIAN_POINT('',(-0.1954,-0.8,-2.39295984553393E-17));
#13777=UNCERTAINTY_MEASURE_WITH_UNIT(LENGTH_MEASURE(0.001),#13822,
'DISTANCE_ACCURACY_VALUE',
'Maximum model space distance between geometric entities at asserted c
onnectivities');
#13782=UNCERTAINTY_MEASURE_WITH_UNIT(LENGTH_MEASURE(0.001),#13822,
'DISTANCE_ACCURACY_VALUE',
'Maximum model space distance between geometric entities at asserted c
onnectivities');
#13816=(
GEOMETRIC_REPRESENTATION_CONTEXT(3)
GLOBAL_UNCERTAINTY_ASSIGNED_CONTEXT((#13777))
GLOBAL_UNIT_ASSIGNED_CONTEXT((#13822,#13824,#13825))
REPRESENTATION_CONTEXT('','3D')
);
#13821=(
GEOMETRIC_REPRESENTATION_CONTEXT(3)
GLOBAL_UNCERTAINTY_ASSIGNED_CONTEXT((#13782))
GLOBAL_UNIT_ASSIGNED_CONTEXT((#13822,#13824,#13825))
REPRESENTATION_CONTEXT('','3D')
);
#13822=(
LENGTH_UNIT()
NAMED_UNIT(*)
SI_UNIT(.CENTI.,.METRE.)
);
#13824=(
NAMED_UNIT(*)
PLANE_ANGLE_UNIT()
SI_UNIT($,.RADIAN.)
);
#13825=(
NAMED_UNIT(*)
SI_UNIT($,.STERADIAN.)
SOLID_ANGLE_UNIT()
);
#13859=SHAPE_DEFINITION_REPRESENTATION(#13902,#14029);
#13902=PRODUCT_DEFINITION_SHAPE('',$,#14068);
#14029=SHAPE_REPRESENTATION('',(#8626),#13816);
#14034=PRODUCT_DEFINITION_CONTEXT('part definition',#14150,'design');
#14068=PRODUCT_DEFINITION('M4x10 Cap Screw','M4x10 Cap Screw',#14106,#14034);
#14106=PRODUCT_DEFINITION_FORMATION('',$,#14185);
#14150=APPLICATION_CONTEXT(
'Core Data for Automotive Mechanical Design Process');
#14151=PRODUCT_CONTEXT('part definition',#14150,'mechanical');
#14185=PRODUCT('M4x10 Cap Screw','M4x10 Cap Screw','M4x10 Cap Screw',(#14151));
#14193=PRESENTATION_STYLE_ASSIGNMENT((#14198));
#14198=SURFACE_STYLE_USAGE(.BOTH.,#14203);
#14203=SURFACE_SIDE_STYLE('',(#14208));
#14208=SURFACE_STYLE_FILL_AREA(#14213);
#14213=FILL_AREA_STYLE('CAD Library Painted - Graphite',(#14218));
#14218=FILL_AREA_STYLE_COLOUR('CAD Library Painted - Graphite',#14223);
#14223=COLOUR_RGB('CAD Library Painted - Graphite',0.168627450980392,0.192156862745098,
0.231372549019608);
ENDSEC;
END-ISO-10303-21;
